ISO-10303-21;
HEADER;
/* Generated by software containing ST-Developer
 * from STEP Tools, Inc. (www.steptools.com) 
 */

FILE_DESCRIPTION(
/* description */ ('Manual rail carriage with stops'),
/* implementation_level */ '2;1');

FILE_NAME(
/* name */ 'Cap Screw - M5x20.step',
/* time_stamp */ '2026-10-27T18:54:27-07:00',
/* author */ (''),
/* organization */ (''),
/* preprocessor_version */ 'ST-DEVELOPER v20.2',
/* originating_system */ 'Autodesk Translation Framework v15.17.0.0',
/* authorisation */ '');

FILE_SCHEMA (('AUTOMOTIVE_DESIGN { 1 0 10303 214 3 1 1 }'));
ENDSEC;

DATA;
#10=MECHANICAL_DESIGN_GEOMETRIC_PRESENTATION_REPRESENTATION('',(#288),#8499);
#219=CONICAL_SURFACE('',#5526,0.4,0.785398163397448);
#220=CONICAL_SURFACE('',#5530,0.41,0.785398163397448);
#221=CONICAL_SURFACE('',#5534,0.26,0.463647609000806);
#222=CONICAL_SURFACE('',#5538,0.225,0.785398163397448);
#229=ORIENTED_CLOSED_SHELL('',*,#4959,.F.);
#233=BREP_WITH_VOIDS('Body1',#4958,(#229));
#252=SHAPE_REPRESENTATION_RELATIONSHIP('SRR','None',#8617,#270);
#270=ADVANCED_BREP_SHAPE_REPRESENTATION('',(#233),#8496);
#288=STYLED_ITEM('',(#8795),#233);
#376=FACE_BOUND('',#1145,.T.);
#553=PLANE('',#5524);
#554=PLANE('',#5532);
#555=PLANE('',#5540);
#556=PLANE('',#5541);
#557=PLANE('',#5542);
#558=PLANE('',#5543);
#559=PLANE('',#5544);
#560=PLANE('',#5545);
#561=PLANE('',#5546);
#562=PLANE('',#5547);
#563=PLANE('',#5548);
#804=FACE_OUTER_BOUND('',#1140,.T.);
#805=FACE_OUTER_BOUND('',#1141,.T.);
#806=FACE_OUTER_BOUND('',#1142,.T.);
#807=FACE_OUTER_BOUND('',#1143,.T.);
#808=FACE_OUTER_BOUND('',#1144,.T.);
#809=FACE_OUTER_BOUND('',#1146,.T.);
#810=FACE_OUTER_BOUND('',#1147,.T.);
#811=FACE_OUTER_BOUND('',#1148,.T.);
#812=FACE_OUTER_BOUND('',#1149,.T.);
#813=FACE_OUTER_BOUND('',#1150,.T.);
#814=FACE_OUTER_BOUND('',#1151,.T.);
#815=FACE_OUTER_BOUND('',#1152,.T.);
#816=FACE_OUTER_BOUND('',#1153,.T.);
#817=FACE_OUTER_BOUND('',#1154,.T.);
#818=FACE_OUTER_BOUND('',#1155,.T.);
#819=FACE_OUTER_BOUND('',#1156,.T.);
#820=FACE_OUTER_BOUND('',#1157,.T.);
#1140=EDGE_LOOP('',(#4484));
#1141=EDGE_LOOP('',(#4485,#4486,#4487,#4488));
#1142=EDGE_LOOP('',(#4489,#4490,#4491,#4492));
#1143=EDGE_LOOP('',(#4493,#4494,#4495,#4496));
#1144=EDGE_LOOP('',(#4497));
#1145=EDGE_LOOP('',(#4498));
#1146=EDGE_LOOP('',(#4499,#4500,#4501,#4502));
#1147=EDGE_LOOP('',(#4503,#4504,#4505,#4506));
#1148=EDGE_LOOP('',(#4507,#4508,#4509,#4510));
#1149=EDGE_LOOP('',(#4511));
#1150=EDGE_LOOP('',(#4512,#4513,#4514,#4515));
#1151=EDGE_LOOP('',(#4516,#4517,#4518,#4519));
#1152=EDGE_LOOP('',(#4520,#4521,#4522,#4523));
#1153=EDGE_LOOP('',(#4524,#4525,#4526,#4527));
#1154=EDGE_LOOP('',(#4528,#4529,#4530,#4531));
#1155=EDGE_LOOP('',(#4532,#4533,#4534,#4535));
#1156=EDGE_LOOP('',(#4536,#4537,#4538,#4539,#4540,#4541));
#1157=EDGE_LOOP('',(#4542,#4543,#4544,#4545,#4546,#4547));
#1632=LINE('',#8259,#2132);
#1633=LINE('',#8263,#2133);
#1634=LINE('',#8267,#2134);
#1635=LINE('',#8274,#2135);
#1636=LINE('',#8278,#2136);
#1637=LINE('',#8282,#2137);
#1638=LINE('',#8287,#2138);
#1639=LINE('',#8289,#2139);
#1640=LINE('',#8291,#2140);
#1641=LINE('',#8292,#2141);
#1642=LINE('',#8295,#2142);
#1643=LINE('',#8297,#2143);
#1644=LINE('',#8298,#2144);
#1645=LINE('',#8301,#2145);
#1646=LINE('',#8303,#2146);
#1647=LINE('',#8304,#2147);
#1648=LINE('',#8307,#2148);
#1649=LINE('',#8309,#2149);
#1650=LINE('',#8310,#2150);
#1651=LINE('',#8313,#2151);
#1652=LINE('',#8315,#2152);
#1653=LINE('',#8316,#2153);
#1654=LINE('',#8318,#2154);
#1655=LINE('',#8319,#2155);
#2132=VECTOR('',#6813,0.4);
#2133=VECTOR('',#6818,0.425);
#2134=VECTOR('',#6823,0.41);
#2135=VECTOR('',#6832,0.26);
#2136=VECTOR('',#6837,0.25);
#2137=VECTOR('',#6842,0.225);
#2138=VECTOR('',#6847,1.);
#2139=VECTOR('',#6848,1.);
#2140=VECTOR('',#6849,1.);
#2141=VECTOR('',#6850,1.);
#2142=VECTOR('',#6853,1.);
#2143=VECTOR('',#6854,1.);
#2144=VECTOR('',#6855,1.);
#2145=VECTOR('',#6858,1.);
#2146=VECTOR('',#6859,1.);
#2147=VECTOR('',#6860,1.);
#2148=VECTOR('',#6863,1.);
#2149=VECTOR('',#6864,1.);
#2150=VECTOR('',#6865,1.);
#2151=VECTOR('',#6868,1.);
#2152=VECTOR('',#6869,1.);
#2153=VECTOR('',#6870,1.);
#2154=VECTOR('',#6873,1.);
#2155=VECTOR('',#6874,1.);
#2292=CIRCLE('',#5525,0.375);
#2293=CIRCLE('',#5527,0.425);
#2294=CIRCLE('',#5529,0.425);
#2295=CIRCLE('',#5531,0.395);
#2296=CIRCLE('',#5533,0.27);
#2297=CIRCLE('',#5535,0.24505);
#2298=CIRCLE('',#5537,0.24505);
#2299=CIRCLE('',#5539,0.2);
#2684=VERTEX_POINT('',#8254);
#2685=VERTEX_POINT('',#8257);
#2686=VERTEX_POINT('',#8261);
#2687=VERTEX_POINT('',#8265);
#2688=VERTEX_POINT('',#8269);
#2689=VERTEX_POINT('',#8272);
#2690=VERTEX_POINT('',#8276);
#2691=VERTEX_POINT('',#8280);
#2692=VERTEX_POINT('',#8285);
#2693=VERTEX_POINT('',#8286);
#2694=VERTEX_POINT('',#8288);
#2695=VERTEX_POINT('',#8290);
#2696=VERTEX_POINT('',#8294);
#2697=VERTEX_POINT('',#8296);
#2698=VERTEX_POINT('',#8300);
#2699=VERTEX_POINT('',#8302);
#2700=VERTEX_POINT('',#8306);
#2701=VERTEX_POINT('',#8308);
#2702=VERTEX_POINT('',#8312);
#2703=VERTEX_POINT('',#8314);
#3290=EDGE_CURVE('',#2684,#2684,#2292,.T.);
#3291=EDGE_CURVE('',#2685,#2685,#2293,.T.);
#3292=EDGE_CURVE('',#2685,#2684,#1632,.T.);
#3293=EDGE_CURVE('',#2686,#2686,#2294,.T.);
#3294=EDGE_CURVE('',#2686,#2685,#1633,.T.);
#3295=EDGE_CURVE('',#2687,#2687,#2295,.T.);
#3296=EDGE_CURVE('',#2687,#2686,#1634,.T.);
#3297=EDGE_CURVE('',#2688,#2688,#2296,.T.);
#3298=EDGE_CURVE('',#2689,#2689,#2297,.F.);
#3299=EDGE_CURVE('',#2689,#2688,#1635,.T.);
#3300=EDGE_CURVE('',#2690,#2690,#2298,.F.);
#3301=EDGE_CURVE('',#2690,#2689,#1636,.T.);
#3302=EDGE_CURVE('',#2691,#2691,#2299,.T.);
#3303=EDGE_CURVE('',#2691,#2690,#1637,.T.);
#3304=EDGE_CURVE('',#2692,#2693,#1638,.T.);
#3305=EDGE_CURVE('',#2693,#2694,#1639,.T.);
#3306=EDGE_CURVE('',#2694,#2695,#1640,.T.);
#3307=EDGE_CURVE('',#2692,#2695,#1641,.T.);
#3308=EDGE_CURVE('',#2693,#2696,#1642,.T.);
#3309=EDGE_CURVE('',#2696,#2697,#1643,.T.);
#3310=EDGE_CURVE('',#2697,#2694,#1644,.T.);
#3311=EDGE_CURVE('',#2696,#2698,#1645,.T.);
#3312=EDGE_CURVE('',#2698,#2699,#1646,.T.);
#3313=EDGE_CURVE('',#2699,#2697,#1647,.T.);
#3314=EDGE_CURVE('',#2698,#2700,#1648,.T.);
#3315=EDGE_CURVE('',#2700,#2701,#1649,.T.);
#3316=EDGE_CURVE('',#2701,#2699,#1650,.T.);
#3317=EDGE_CURVE('',#2700,#2702,#1651,.T.);
#3318=EDGE_CURVE('',#2702,#2703,#1652,.T.);
#3319=EDGE_CURVE('',#2703,#2701,#1653,.T.);
#3320=EDGE_CURVE('',#2702,#2692,#1654,.T.);
#3321=EDGE_CURVE('',#2695,#2703,#1655,.T.);
#4484=ORIENTED_EDGE('',*,*,#3290,.F.);
#4485=ORIENTED_EDGE('',*,*,#3291,.F.);
#4486=ORIENTED_EDGE('',*,*,#3292,.T.);
#4487=ORIENTED_EDGE('',*,*,#3290,.T.);
#4488=ORIENTED_EDGE('',*,*,#3292,.F.);
#4489=ORIENTED_EDGE('',*,*,#3293,.F.);
#4490=ORIENTED_EDGE('',*,*,#3294,.T.);
#4491=ORIENTED_EDGE('',*,*,#3291,.T.);
#4492=ORIENTED_EDGE('',*,*,#3294,.F.);
#4493=ORIENTED_EDGE('',*,*,#3295,.F.);
#4494=ORIENTED_EDGE('',*,*,#3296,.T.);
#4495=ORIENTED_EDGE('',*,*,#3293,.T.);
#4496=ORIENTED_EDGE('',*,*,#3296,.F.);
#4497=ORIENTED_EDGE('',*,*,#3295,.T.);
#4498=ORIENTED_EDGE('',*,*,#3297,.F.);
#4499=ORIENTED_EDGE('',*,*,#3298,.F.);
#4500=ORIENTED_EDGE('',*,*,#3299,.T.);
#4501=ORIENTED_EDGE('',*,*,#3297,.T.);
#4502=ORIENTED_EDGE('',*,*,#3299,.F.);
#4503=ORIENTED_EDGE('',*,*,#3300,.F.);
#4504=ORIENTED_EDGE('',*,*,#3301,.T.);
#4505=ORIENTED_EDGE('',*,*,#3298,.T.);
#4506=ORIENTED_EDGE('',*,*,#3301,.F.);
#4507=ORIENTED_EDGE('',*,*,#3302,.F.);
#4508=ORIENTED_EDGE('',*,*,#3303,.T.);
#4509=ORIENTED_EDGE('',*,*,#3300,.T.);
#4510=ORIENTED_EDGE('',*,*,#3303,.F.);
#4511=ORIENTED_EDGE('',*,*,#3302,.T.);
#4512=ORIENTED_EDGE('',*,*,#3304,.T.);
#4513=ORIENTED_EDGE('',*,*,#3305,.T.);
#4514=ORIENTED_EDGE('',*,*,#3306,.T.);
#4515=ORIENTED_EDGE('',*,*,#3307,.F.);
#4516=ORIENTED_EDGE('',*,*,#3308,.T.);
#4517=ORIENTED_EDGE('',*,*,#3309,.T.);
#4518=ORIENTED_EDGE('',*,*,#3310,.T.);
#4519=ORIENTED_EDGE('',*,*,#3305,.F.);
#4520=ORIENTED_EDGE('',*,*,#3311,.T.);
#4521=ORIENTED_EDGE('',*,*,#3312,.T.);
#4522=ORIENTED_EDGE('',*,*,#3313,.T.);
#4523=ORIENTED_EDGE('',*,*,#3309,.F.);
#4524=ORIENTED_EDGE('',*,*,#3314,.T.);
#4525=ORIENTED_EDGE('',*,*,#3315,.T.);
#4526=ORIENTED_EDGE('',*,*,#3316,.T.);
#4527=ORIENTED_EDGE('',*,*,#3312,.F.);
#4528=ORIENTED_EDGE('',*,*,#3317,.T.);
#4529=ORIENTED_EDGE('',*,*,#3318,.T.);
#4530=ORIENTED_EDGE('',*,*,#3319,.T.);
#4531=ORIENTED_EDGE('',*,*,#3315,.F.);
#4532=ORIENTED_EDGE('',*,*,#3320,.T.);
#4533=ORIENTED_EDGE('',*,*,#3307,.T.);
#4534=ORIENTED_EDGE('',*,*,#3321,.T.);
#4535=ORIENTED_EDGE('',*,*,#3318,.F.);
#4536=ORIENTED_EDGE('',*,*,#3320,.F.);
#4537=ORIENTED_EDGE('',*,*,#3317,.F.);
#4538=ORIENTED_EDGE('',*,*,#3314,.F.);
#4539=ORIENTED_EDGE('',*,*,#3311,.F.);
#4540=ORIENTED_EDGE('',*,*,#3308,.F.);
#4541=ORIENTED_EDGE('',*,*,#3304,.F.);
#4542=ORIENTED_EDGE('',*,*,#3321,.F.);
#4543=ORIENTED_EDGE('',*,*,#3306,.F.);
#4544=ORIENTED_EDGE('',*,*,#3310,.F.);
#4545=ORIENTED_EDGE('',*,*,#3313,.F.);
#4546=ORIENTED_EDGE('',*,*,#3316,.F.);
#4547=ORIENTED_EDGE('',*,*,#3319,.F.);
#4670=CYLINDRICAL_SURFACE('',#5528,0.425);
#4671=CYLINDRICAL_SURFACE('',#5536,0.24505);
#4903=ADVANCED_FACE('',(#804),#553,.T.);
#4904=ADVANCED_FACE('',(#805),#219,.T.);
#4905=ADVANCED_FACE('',(#806),#4670,.T.);
#4906=ADVANCED_FACE('',(#807),#220,.T.);
#4907=ADVANCED_FACE('',(#808,#376),#554,.T.);
#4908=ADVANCED_FACE('',(#809),#221,.T.);
#4909=ADVANCED_FACE('',(#810),#4671,.T.);
#4910=ADVANCED_FACE('',(#811),#222,.T.);
#4911=ADVANCED_FACE('',(#812),#555,.T.);
#4912=ADVANCED_FACE('',(#813),#556,.F.);
#4913=ADVANCED_FACE('',(#814),#557,.F.);
#4914=ADVANCED_FACE('',(#815),#558,.F.);
#4915=ADVANCED_FACE('',(#816),#559,.F.);
#4916=ADVANCED_FACE('',(#817),#560,.F.);
#4917=ADVANCED_FACE('',(#818),#561,.F.);
#4918=ADVANCED_FACE('',(#819),#562,.F.);
#4919=ADVANCED_FACE('',(#820),#563,.F.);
#4958=CLOSED_SHELL('',(#4903,#4904,#4905,#4906,#4907,#4908,#4909,#4910,
#4911));
#4959=CLOSED_SHELL('',(#4912,#4913,#4914,#4915,#4916,#4917,#4918,#4919));
#5523=AXIS2_PLACEMENT_3D('',#8252,#6803,#6804);
#5524=AXIS2_PLACEMENT_3D('',#8253,#6805,#6806);
#5525=AXIS2_PLACEMENT_3D('',#8255,#6807,#6808);
#5526=AXIS2_PLACEMENT_3D('',#8256,#6809,#6810);
#5527=AXIS2_PLACEMENT_3D('',#8258,#6811,#6812);
#5528=AXIS2_PLACEMENT_3D('',#8260,#6814,#6815);
#5529=AXIS2_PLACEMENT_3D('',#8262,#6816,#6817);
#5530=AXIS2_PLACEMENT_3D('',#8264,#6819,#6820);
#5531=AXIS2_PLACEMENT_3D('',#8266,#6821,#6822);
#5532=AXIS2_PLACEMENT_3D('',#8268,#6824,#6825);
#5533=AXIS2_PLACEMENT_3D('',#8270,#6826,#6827);
#5534=AXIS2_PLACEMENT_3D('',#8271,#6828,#6829);
#5535=AXIS2_PLACEMENT_3D('',#8273,#6830,#6831);
#5536=AXIS2_PLACEMENT_3D('',#8275,#6833,#6834);
#5537=AXIS2_PLACEMENT_3D('',#8277,#6835,#6836);
#5538=AXIS2_PLACEMENT_3D('',#8279,#6838,#6839);
#5539=AXIS2_PLACEMENT_3D('',#8281,#6840,#6841);
#5540=AXIS2_PLACEMENT_3D('',#8283,#6843,#6844);
#5541=AXIS2_PLACEMENT_3D('',#8284,#6845,#6846);
#5542=AXIS2_PLACEMENT_3D('',#8293,#6851,#6852);
#5543=AXIS2_PLACEMENT_3D('',#8299,#6856,#6857);
#5544=AXIS2_PLACEMENT_3D('',#8305,#6861,#6862);
#5545=AXIS2_PLACEMENT_3D('',#8311,#6866,#6867);
#5546=AXIS2_PLACEMENT_3D('',#8317,#6871,#6872);
#5547=AXIS2_PLACEMENT_3D('',#8320,#6875,#6876);
#5548=AXIS2_PLACEMENT_3D('',#8321,#6877,#6878);
#6803=DIRECTION('axis',(0.,0.,1.));
#6804=DIRECTION('refdir',(1.,0.,0.));
#6805=DIRECTION('center_axis',(0.,1.,0.));
#6806=DIRECTION('ref_axis',(0.,0.,1.));
#6807=DIRECTION('center_axis',(0.,-1.,0.));
#6808=DIRECTION('ref_axis',(1.,0.,0.));
#6809=DIRECTION('center_axis',(0.,-1.,0.));
#6810=DIRECTION('ref_axis',(1.,0.,0.));
#6811=DIRECTION('center_axis',(0.,-1.,0.));
#6812=DIRECTION('ref_axis',(1.,0.,0.));
#6813=DIRECTION('',(0.707106781186548,0.707106781186547,8.65956056235493E-17));
#6814=DIRECTION('center_axis',(0.,-1.,0.));
#6815=DIRECTION('ref_axis',(1.,0.,0.));
#6816=DIRECTION('center_axis',(0.,-1.,0.));
#6817=DIRECTION('ref_axis',(1.,0.,0.));
#6818=DIRECTION('',(0.,1.,0.));
#6819=DIRECTION('center_axis',(0.,1.,0.));
#6820=DIRECTION('ref_axis',(1.,0.,0.));
#6821=DIRECTION('center_axis',(0.,-1.,0.));
#6822=DIRECTION('ref_axis',(1.,0.,0.));
#6823=DIRECTION('',(-0.707106781186547,0.707106781186548,-8.65956056235493E-17));
#6824=DIRECTION('center_axis',(0.,-1.,0.));
#6825=DIRECTION('ref_axis',(0.,0.,-1.));
#6826=DIRECTION('center_axis',(0.,-1.,0.));
#6827=DIRECTION('ref_axis',(1.,0.,0.));
#6828=DIRECTION('center_axis',(0.,1.,0.));
#6829=DIRECTION('ref_axis',(1.,0.,0.));
#6830=DIRECTION('center_axis',(0.,1.,0.));
#6831=DIRECTION('ref_axis',(1.,0.,0.));
#6832=DIRECTION('',(-0.447213595499958,0.894427190999916,-5.47678698264203E-17));
#6833=DIRECTION('center_axis',(0.,-1.,0.));
#6834=DIRECTION('ref_axis',(1.,0.,0.));
#6835=DIRECTION('center_axis',(0.,1.,0.));
#6836=DIRECTION('ref_axis',(1.,0.,0.));
#6837=DIRECTION('',(0.,1.,0.));
#6838=DIRECTION('center_axis',(0.,1.,0.));
#6839=DIRECTION('ref_axis',(1.,0.,0.));
#6840=DIRECTION('center_axis',(0.,-1.,0.));
#6841=DIRECTION('ref_axis',(1.,0.,0.));
#6842=DIRECTION('',(-0.707106781186547,0.707106781186548,-8.65956056235493E-17));
#6843=DIRECTION('center_axis',(0.,-1.,0.));
#6844=DIRECTION('ref_axis',(0.,0.,-1.));
#6845=DIRECTION('center_axis',(0.866025403784439,0.,-0.5));
#6846=DIRECTION('ref_axis',(0.5,0.,0.866025403784439));
#6847=DIRECTION('',(-0.5,0.,-0.866025403784439));
#6848=DIRECTION('',(0.,-1.,0.));
#6849=DIRECTION('',(0.5,0.,0.866025403784439));
#6850=DIRECTION('',(0.,-1.,0.));
#6851=DIRECTION('center_axis',(1.20185167898973E-16,0.,-1.));
#6852=DIRECTION('ref_axis',(1.,0.,1.20185167898973E-16));
#6853=DIRECTION('',(-1.,0.,-1.20185167898973E-16));
#6854=DIRECTION('',(0.,-1.,0.));
#6855=DIRECTION('',(1.,0.,1.20185167898973E-16));
#6856=DIRECTION('center_axis',(-0.866025403784439,0.,-0.5));
#6857=DIRECTION('ref_axis',(0.5,0.,-0.866025403784439));
#6858=DIRECTION('',(-0.5,0.,0.866025403784439));
#6859=DIRECTION('',(0.,-1.,0.));
#6860=DIRECTION('',(0.5,0.,-0.866025403784439));
#6861=DIRECTION('center_axis',(-0.866025403784439,0.,0.5));
#6862=DIRECTION('ref_axis',(-0.5,0.,-0.866025403784439));
#6863=DIRECTION('',(0.5,0.,0.866025403784439));
#6864=DIRECTION('',(0.,-1.,0.));
#6865=DIRECTION('',(-0.5,0.,-0.866025403784439));
#6866=DIRECTION('center_axis',(-2.40370335797945E-16,0.,1.));
#6867=DIRECTION('ref_axis',(-1.,0.,-2.40370335797945E-16));
#6868=DIRECTION('',(1.,0.,2.40370335797945E-16));
#6869=DIRECTION('',(0.,-1.,0.));
#6870=DIRECTION('',(-1.,0.,-2.40370335797945E-16));
#6871=DIRECTION('center_axis',(0.866025403784439,0.,0.5));
#6872=DIRECTION('ref_axis',(-0.5,0.,0.866025403784439));
#6873=DIRECTION('',(0.5,0.,-0.866025403784439));
#6874=DIRECTION('',(-0.5,0.,0.866025403784439));
#6875=DIRECTION('center_axis',(0.,1.,0.));
#6876=DIRECTION('ref_axis',(1.,0.,0.));
#6877=DIRECTION('center_axis',(0.,-1.,0.));
#6878=DIRECTION('ref_axis',(0.,0.,-1.));
#8252=CARTESIAN_POINT('',(0.,0.,0.));
#8253=CARTESIAN_POINT('Origin',(0.375,0.5,0.));
#8254=CARTESIAN_POINT('',(-0.375,0.5,-4.59242549680257E-17));
#8255=CARTESIAN_POINT('Origin',(0.,0.5,0.));
#8256=CARTESIAN_POINT('Origin',(0.,0.475,0.));
#8257=CARTESIAN_POINT('',(-0.425,0.45,-5.20474889637625E-17));
#8258=CARTESIAN_POINT('Origin',(0.,0.45,0.));
#8259=CARTESIAN_POINT('',(-0.4,0.475,-4.89858719658941E-17));
#8260=CARTESIAN_POINT('Origin',(0.,0.24,0.));
#8261=CARTESIAN_POINT('',(-0.425,0.0299999999999998,-5.20474889637625E-17));
#8262=CARTESIAN_POINT('Origin',(0.,0.0299999999999998,0.));
#8263=CARTESIAN_POINT('',(-0.425,0.24,-5.20474889637625E-17));
#8264=CARTESIAN_POINT('Origin',(0.,0.0150000000000001,0.));
#8265=CARTESIAN_POINT('',(-0.395,4.85722573273506E-17,-4.83735485663204E-17));
#8266=CARTESIAN_POINT('Origin',(0.,0.,0.));
#8267=CARTESIAN_POINT('',(-0.41,0.0150000000000001,-5.02105187650415E-17));
#8268=CARTESIAN_POINT('Origin',(0.27,0.,0.));
#8269=CARTESIAN_POINT('',(-0.27,0.,-3.30654635769785E-17));
#8270=CARTESIAN_POINT('Origin',(0.,0.,0.));
#8271=CARTESIAN_POINT('Origin',(0.,-0.02,0.));
#8272=CARTESIAN_POINT('',(-0.24505,-0.0498999999999999,3.00099698131059E-17));
#8273=CARTESIAN_POINT('Origin',(0.,-0.0498999999999999,0.));
#8274=CARTESIAN_POINT('',(-0.26,-0.02,-3.18408167778312E-17));
#8275=CARTESIAN_POINT('Origin',(0.,-0.995,0.));
#8276=CARTESIAN_POINT('',(-0.24505,-1.95495,3.00099698131059E-17));
#8277=CARTESIAN_POINT('Origin',(0.,-1.95495,0.));
#8278=CARTESIAN_POINT('',(-0.24505,-0.995,-3.00099698131059E-17));
#8279=CARTESIAN_POINT('Origin',(0.,-1.975,0.));
#8280=CARTESIAN_POINT('',(-0.2,-2.,-2.44929359829471E-17));
#8281=CARTESIAN_POINT('Origin',(0.,-2.,0.));
#8282=CARTESIAN_POINT('',(-0.225,-1.975,-2.75545529808154E-17));
#8283=CARTESIAN_POINT('Origin',(0.,-2.,0.));
#8284=CARTESIAN_POINT('Origin',(0.115470053837925,-0.5,-0.2));
#8285=CARTESIAN_POINT('',(0.23094010767585,-0.5,0.));
#8286=CARTESIAN_POINT('',(0.115470053837925,-0.5,-0.2));
#8287=CARTESIAN_POINT('',(0.23094010767585,-0.5,0.));
#8288=CARTESIAN_POINT('',(0.115470053837925,-0.8,-0.2));
#8289=CARTESIAN_POINT('',(0.115470053837925,-0.5,-0.2));
#8290=CARTESIAN_POINT('',(0.23094010767585,-0.8,0.));
#8291=CARTESIAN_POINT('',(0.23094010767585,-0.8,0.));
#8292=CARTESIAN_POINT('',(0.23094010767585,-0.5,0.));
#8293=CARTESIAN_POINT('Origin',(-0.115470053837925,-0.5,-0.2));
#8294=CARTESIAN_POINT('',(-0.115470053837925,-0.5,-0.2));
#8295=CARTESIAN_POINT('',(0.115470053837925,-0.5,-0.2));
#8296=CARTESIAN_POINT('',(-0.115470053837925,-0.8,-0.2));
#8297=CARTESIAN_POINT('',(-0.115470053837925,-0.5,-0.2));
#8298=CARTESIAN_POINT('',(0.115470053837925,-0.8,-0.2));
#8299=CARTESIAN_POINT('Origin',(-0.23094010767585,-0.5,-2.77555756156289E-17));
#8300=CARTESIAN_POINT('',(-0.23094010767585,-0.5,-2.82820063659975E-17));
#8301=CARTESIAN_POINT('',(-0.115470053837925,-0.5,-0.2));
#8302=CARTESIAN_POINT('',(-0.23094010767585,-0.8,-2.77555756156289E-17));
#8303=CARTESIAN_POINT('',(-0.23094010767585,-0.5,-2.82820063659975E-17));
#8304=CARTESIAN_POINT('',(-0.115470053837925,-0.8,-0.2));
#8305=CARTESIAN_POINT('Origin',(-0.115470053837925,-0.5,0.2));
#8306=CARTESIAN_POINT('',(-0.115470053837925,-0.5,0.2));
#8307=CARTESIAN_POINT('',(-0.23094010767585,-0.5,-2.82820063659975E-17));
#8308=CARTESIAN_POINT('',(-0.115470053837925,-0.8,0.2));
#8309=CARTESIAN_POINT('',(-0.115470053837925,-0.5,0.2));
#8310=CARTESIAN_POINT('',(-0.23094010767585,-0.8,-2.82820063659975E-17));
#8311=CARTESIAN_POINT('Origin',(0.115470053837925,-0.5,0.2));
#8312=CARTESIAN_POINT('',(0.115470053837925,-0.5,0.2));
#8313=CARTESIAN_POINT('',(-0.115470053837925,-0.5,0.2));
#8314=CARTESIAN_POINT('',(0.115470053837925,-0.8,0.2));
#8315=CARTESIAN_POINT('',(0.115470053837925,-0.5,0.2));
#8316=CARTESIAN_POINT('',(-0.115470053837925,-0.8,0.2));
#8317=CARTESIAN_POINT('Origin',(0.23094010767585,-0.5,0.));
#8318=CARTESIAN_POINT('',(0.115470053837925,-0.5,0.2));
#8319=CARTESIAN_POINT('',(0.115470053837925,-0.8,0.2));
#8320=CARTESIAN_POINT('Origin',(0.,-0.5,0.));
#8321=CARTESIAN_POINT('Origin',(0.,-0.8,0.));
#8473=UNCERTAINTY_MEASURE_WITH_UNIT(LENGTH_MEASURE(0.001),#8500,
'DISTANCE_ACCURACY_VALUE',
'Maximum model space distance between geometric entities at asserted c
onnectivities');
#8476=UNCERTAINTY_MEASURE_WITH_UNIT(LENGTH_MEASURE(0.001),#8500,
'DISTANCE_ACCURACY_VALUE',
'Maximum model space distance between geometric entities at asserted c
onnectivities');
#8496=(
GEOMETRIC_REPRESENTATION_CONTEXT(3)
GLOBAL_UNCERTAINTY_ASSIGNED_CONTEXT((#8473))
GLOBAL_UNIT_ASSIGNED_CONTEXT((#8500,#8502,#8503))
REPRESENTATION_CONTEXT('','3D')
);
#8499=(
GEOMETRIC_REPRESENTATION_CONTEXT(3)
GLOBAL_UNCERTAINTY_ASSIGNED_CONTEXT((#8476))
GLOBAL_UNIT_ASSIGNED_CONTEXT((#8500,#8502,#8503))
REPRESENTATION_CONTEXT('','3D')
);
#8500=(
LENGTH_UNIT()
NAMED_UNIT(*)
SI_UNIT(.CENTI.,.METRE.)
);
#8502=(
NAMED_UNIT(*)
PLANE_ANGLE_UNIT()
SI_UNIT($,.RADIAN.)
);
#8503=(
NAMED_UNIT(*)
SI_UNIT($,.STERADIAN.)
SOLID_ANGLE_UNIT()
);
#8523=SHAPE_DEFINITION_REPRESENTATION(#8548,#8617);
#8548=PRODUCT_DEFINITION_SHAPE('',$,#8640);
#8617=SHAPE_REPRESENTATION('',(#5523),#8496);
#8620=PRODUCT_DEFINITION_CONTEXT('part definition',#8688,'design');
#8640=PRODUCT_DEFINITION('Cap Screw - M5x20','Cap Screw - M5x20',#8662,
#8620);
#8662=PRODUCT_DEFINITION_FORMATION('',$,#8709);
#8688=APPLICATION_CONTEXT(
'Core Data for Automotive Mechanical Design Process');
#8689=PRODUCT_CONTEXT('part definition',#8688,'mechanical');
#8709=PRODUCT('Cap Screw - M5x20','Cap Screw - M5x20',
'Cap Screw - M5x20',(#8689));
#8789=COLOUR_RGB('Black',0.12,0.14,0.17);
#8790=FILL_AREA_STYLE_COLOUR('',#8789);
#8791=FILL_AREA_STYLE('',(#8790));
#8792=SURFACE_STYLE_FILL_AREA(#8791);
#8793=SURFACE_SIDE_STYLE('',(#8792));
#8794=SURFACE_STYLE_USAGE(.BOTH.,#8793);
#8795=PRESENTATION_STYLE_ASSIGNMENT((#8794));
ENDSEC;
END-ISO-10303-21;
